ISO-10303-21;
HEADER;
/* Generated by software containing ST-Developer
 * from STEP Tools, Inc. (www.steptools.com) 
 */

FILE_DESCRIPTION(
/* description */ ('STEP AP214'),
/* implementation_level */ '2;1');

FILE_NAME(
/* name */ 'Thrust Washer.step',
/* time_stamp */ '2026-11-14T05:50:49-08:00',
/* author */ (''),
/* organization */ (''),
/* preprocessor_version */ 'ST-DEVELOPER v20.2',
/* originating_system */ 'Autodesk Translation Framework v15.17.0.0',
/* authorisation */ '');

FILE_SCHEMA (('AUTOMOTIVE_DESIGN { 1 0 10303 214 3 1 1 }'));
ENDSEC;

DATA;
#10=MECHANICAL_DESIGN_GEOMETRIC_PRESENTATION_REPRESENTATION('',(#160),#9903);
#146=SHAPE_REPRESENTATION_RELATIONSHIP('SRR','None',#9941,#153);
#153=ADVANCED_BREP_SHAPE_REPRESENTATION('',(#167),#9899);
#160=STYLED_ITEM('',(#9983),#167);
#167=MANIFOLD_SOLID_BREP('Body1',#2025);
#181=FACE_BOUND('',#418,.T.);
#182=FACE_BOUND('',#420,.T.);
#212=PLANE('',#2196);
#213=PLANE('',#2197);
#287=FACE_OUTER_BOUND('',#415,.T.);
#288=FACE_OUTER_BOUND('',#416,.T.);
#289=FACE_OUTER_BOUND('',#417,.T.);
#290=FACE_OUTER_BOUND('',#419,.T.);
#415=EDGE_LOOP('',(#1436,#1437,#1438,#1439));
#416=EDGE_LOOP('',(#1440,#1441,#1442,#1443));
#417=EDGE_LOOP('',(#1444));
#418=EDGE_LOOP('',(#1445));
#419=EDGE_LOOP('',(#1446));
#420=EDGE_LOOP('',(#1447));
#533=LINE('',#3023,#669);
#534=LINE('',#3029,#670);
#669=VECTOR('',#2508,7.);
#670=VECTOR('',#2515,12.);
#828=CIRCLE('',#2191,7.);
#829=CIRCLE('',#2192,7.);
#830=CIRCLE('',#2194,12.);
#831=CIRCLE('',#2195,12.);
#899=VERTEX_POINT('',#3020);
#900=VERTEX_POINT('',#3022);
#901=VERTEX_POINT('',#3026);
#902=VERTEX_POINT('',#3028);
#1099=EDGE_CURVE('',#899,#899,#828,.T.);
#1100=EDGE_CURVE('',#899,#900,#533,.T.);
#1101=EDGE_CURVE('',#900,#900,#829,.T.);
#1102=EDGE_CURVE('',#901,#901,#830,.T.);
#1103=EDGE_CURVE('',#901,#902,#534,.T.);
#1104=EDGE_CURVE('',#902,#902,#831,.T.);
#1436=ORIENTED_EDGE('',*,*,#1099,.F.);
#1437=ORIENTED_EDGE('',*,*,#1100,.T.);
#1438=ORIENTED_EDGE('',*,*,#1101,.T.);
#1439=ORIENTED_EDGE('',*,*,#1100,.F.);
#1440=ORIENTED_EDGE('',*,*,#1102,.F.);
#1441=ORIENTED_EDGE('',*,*,#1103,.T.);
#1442=ORIENTED_EDGE('',*,*,#1104,.T.);
#1443=ORIENTED_EDGE('',*,*,#1103,.F.);
#1444=ORIENTED_EDGE('',*,*,#1102,.T.);
#1445=ORIENTED_EDGE('',*,*,#1101,.F.);
#1446=ORIENTED_EDGE('',*,*,#1104,.F.);
#1447=ORIENTED_EDGE('',*,*,#1099,.T.);
#1868=CYLINDRICAL_SURFACE('',#2190,7.);
#1869=CYLINDRICAL_SURFACE('',#2193,12.);
#1939=ADVANCED_FACE('',(#287),#1868,.F.);
#1940=ADVANCED_FACE('',(#288),#1869,.T.);
#1941=ADVANCED_FACE('',(#289,#181),#212,.F.);
#1942=ADVANCED_FACE('',(#290,#182),#213,.T.);
#2025=CLOSED_SHELL('',(#1939,#1940,#1941,#1942));
#2189=AXIS2_PLACEMENT_3D('',#3018,#2502,#2503);
#2190=AXIS2_PLACEMENT_3D('',#3019,#2504,#2505);
#2191=AXIS2_PLACEMENT_3D('',#3021,#2506,#2507);
#2192=AXIS2_PLACEMENT_3D('',#3024,#2509,#2510);
#2193=AXIS2_PLACEMENT_3D('',#3025,#2511,#2512);
#2194=AXIS2_PLACEMENT_3D('',#3027,#2513,#2514);
#2195=AXIS2_PLACEMENT_3D('',#3030,#2516,#2517);
#2196=AXIS2_PLACEMENT_3D('',#3031,#2518,#2519);
#2197=AXIS2_PLACEMENT_3D('',#3032,#2520,#2521);
#2502=DIRECTION('axis',(0.,0.,1.));
#2503=DIRECTION('refdir',(1.,0.,0.));
#2504=DIRECTION('center_axis',(-1.,0.,0.));
#2505=DIRECTION('ref_axis',(0.,0.,1.));
#2506=DIRECTION('center_axis',(-1.,0.,0.));
#2507=DIRECTION('ref_axis',(0.,0.,1.));
#2508=DIRECTION('',(-1.,0.,0.));
#2509=DIRECTION('center_axis',(-1.,0.,0.));
#2510=DIRECTION('ref_axis',(0.,0.,1.));
#2511=DIRECTION('center_axis',(-1.,0.,0.));
#2512=DIRECTION('ref_axis',(0.,0.,1.));
#2513=DIRECTION('center_axis',(-1.,0.,0.));
#2514=DIRECTION('ref_axis',(0.,0.,1.));
#2515=DIRECTION('',(1.,0.,0.));
#2516=DIRECTION('center_axis',(-1.,0.,0.));
#2517=DIRECTION('ref_axis',(0.,0.,1.));
#2518=DIRECTION('center_axis',(1.,0.,0.));
#2519=DIRECTION('ref_axis',(0.,0.,-1.));
#2520=DIRECTION('center_axis',(1.,0.,0.));
#2521=DIRECTION('ref_axis',(0.,0.,-1.));
#3018=CARTESIAN_POINT('',(0.,0.,0.));
#3019=CARTESIAN_POINT('Origin',(-5.,0.,0.));
#3020=CARTESIAN_POINT('',(5.,-8.57252759403147E-16,-7.));
#3021=CARTESIAN_POINT('Origin',(5.,0.,0.));
#3022=CARTESIAN_POINT('',(-5.,-8.57252759403147E-16,-7.));
#3023=CARTESIAN_POINT('',(-5.,-8.57252759403147E-16,-7.));
#3024=CARTESIAN_POINT('Origin',(-5.,0.,0.));
#3025=CARTESIAN_POINT('Origin',(-5.,0.,0.));
#3026=CARTESIAN_POINT('',(-5.,-1.46957615897682E-15,-12.));
#3027=CARTESIAN_POINT('Origin',(-5.,0.,0.));
#3028=CARTESIAN_POINT('',(5.,-1.46957615897682E-15,-12.));
#3029=CARTESIAN_POINT('',(-5.,-1.46957615897682E-15,-12.));
#3030=CARTESIAN_POINT('Origin',(5.,0.,0.));
#3031=CARTESIAN_POINT('Origin',(-5.,0.,0.));
#3032=CARTESIAN_POINT('Origin',(5.,0.,0.));
#9890=UNCERTAINTY_MEASURE_WITH_UNIT(LENGTH_MEASURE(0.01),#9904,
'DISTANCE_ACCURACY_VALUE',
'Maximum model space distance between geometric entities at asserted c
onnectivities');
#9894=UNCERTAINTY_MEASURE_WITH_UNIT(LENGTH_MEASURE(0.01),#9904,
'DISTANCE_ACCURACY_VALUE',
'Maximum model space distance between geometric entities at asserted c
onnectivities');
#9899=(
GEOMETRIC_REPRESENTATION_CONTEXT(3)
GLOBAL_UNCERTAINTY_ASSIGNED_CONTEXT((#9890))
GLOBAL_UNIT_ASSIGNED_CONTEXT((#9904,#9906,#9907))
REPRESENTATION_CONTEXT('','3D')
);
#9903=(
GEOMETRIC_REPRESENTATION_CONTEXT(3)
GLOBAL_UNCERTAINTY_ASSIGNED_CONTEXT((#9894))
GLOBAL_UNIT_ASSIGNED_CONTEXT((#9904,#9906,#9907))
REPRESENTATION_CONTEXT('','3D')
);
#9904=(
LENGTH_UNIT()
NAMED_UNIT(*)
SI_UNIT(.MILLI.,.METRE.)
);
#9906=(
NAMED_UNIT(*)
PLANE_ANGLE_UNIT()
SI_UNIT($,.RADIAN.)
);
#9907=(
NAMED_UNIT(*)
SI_UNIT($,.STERADIAN.)
SOLID_ANGLE_UNIT()
);
#9912=SHAPE_DEFINITION_REPRESENTATION(#9920,#9941);
#9920=PRODUCT_DEFINITION_SHAPE('',$,#9950);
#9941=SHAPE_REPRESENTATION('',(#2189),#9899);
#9945=PRODUCT_DEFINITION_CONTEXT('part definition',#9971,'design');
#9950=PRODUCT_DEFINITION('Thrust washer','Thrust Washer',#9958,#9945);
#9958=PRODUCT_DEFINITION_FORMATION('',$,#9977);
#9971=APPLICATION_CONTEXT(
'Core Data for Automotive Mechanical Design Process');
#9972=PRODUCT_CONTEXT('part definition',#9971,'mechanical');
#9977=PRODUCT('Thrust washer','Thrust Washer',$,(#9972));
#9983=PRESENTATION_STYLE_ASSIGNMENT((#9988));
#9988=SURFACE_STYLE_USAGE(.BOTH.,#9993);
#9993=SURFACE_SIDE_STYLE('',(#9998));
#9998=SURFACE_STYLE_FILL_AREA(#10003);
#10003=FILL_AREA_STYLE('Opaque(61,176,222)',(#10008));
#10008=FILL_AREA_STYLE_COLOUR('Opaque(61,176,222)',#10013);
#10013=COLOUR_RGB('Opaque(61,176,222)',0.23921568627451,0.690196078431373,
0.870588235294118);
ENDSEC;
END-ISO-10303-21;
